ISO-10303-21;
HEADER;
/* Generated by software containing ST-Developer
 * from STEP Tools, Inc. (www.steptools.com) 
 */

FILE_DESCRIPTION(
/* description */ ('STEP AP214'),
/* implementation_level */ '2;1');

FILE_NAME(
/* name */ 'High Strength Hex Head Bolt DIN 6914 M16 x 60.step',
/* time_stamp */ '2026-11-14T07:13:32-08:00',
/* author */ (''),
/* organization */ (''),
/* preprocessor_version */ 'ST-DEVELOPER v20.2',
/* originating_system */ 'Autodesk Translation Framework v15.17.0.0',
/* authorisation */ '');

FILE_SCHEMA (('AUTOMOTIVE_DESIGN { 1 0 10303 214 3 1 1 }'));
ENDSEC;

DATA;
#10=MECHANICAL_DESIGN_GEOMETRIC_PRESENTATION_REPRESENTATION('',(#1377),#32903);
#538=(
BOUNDED_CURVE()
B_SPLINE_CURVE(2,(#32588,#32589,#32590),.UNSPECIFIED.,.F.,.F.)
B_SPLINE_CURVE_WITH_KNOTS((3,3),(-3.03150105849453,-1.74744567255227),
 .UNSPECIFIED.)
CURVE()
GEOMETRIC_REPRESENTATION_ITEM()
RATIONAL_B_SPLINE_CURVE((1.66716031106357,1.66716031106357,1.54746358611627))
REPRESENTATION_ITEM('')
);
#539=(
BOUNDED_CURVE()
B_SPLINE_CURVE(2,(#32591,#32592,#32593),.UNSPECIFIED.,.F.,.F.)
B_SPLINE_CURVE_WITH_KNOTS((3,3),(-4.3155564444368,-3.03150105849454),
 .UNSPECIFIED.)
CURVE()
GEOMETRIC_REPRESENTATION_ITEM()
RATIONAL_B_SPLINE_CURVE((1.54746358611627,1.66716031106357,1.66716031106357))
REPRESENTATION_ITEM('')
);
#540=(
BOUNDED_CURVE()
B_SPLINE_CURVE(2,(#32596,#32597,#32598),.UNSPECIFIED.,.F.,.F.)
B_SPLINE_CURVE_WITH_KNOTS((3,3),(-3.03150105849453,-1.74744567255227),
 .UNSPECIFIED.)
CURVE()
GEOMETRIC_REPRESENTATION_ITEM()
RATIONAL_B_SPLINE_CURVE((1.66716031106357,1.66716031106357,1.54746358611627))
REPRESENTATION_ITEM('')
);
#541=(
BOUNDED_CURVE()
B_SPLINE_CURVE(2,(#32599,#32600,#32601),.UNSPECIFIED.,.F.,.F.)
B_SPLINE_CURVE_WITH_KNOTS((3,3),(-4.31555644443679,-3.03150105849453),
 .UNSPECIFIED.)
CURVE()
GEOMETRIC_REPRESENTATION_ITEM()
RATIONAL_B_SPLINE_CURVE((1.54746358611627,1.66716031106357,1.66716031106357))
REPRESENTATION_ITEM('')
);
#542=(
BOUNDED_CURVE()
B_SPLINE_CURVE(2,(#32604,#32605,#32606),.UNSPECIFIED.,.F.,.F.)
B_SPLINE_CURVE_WITH_KNOTS((3,3),(-4.3155564444368,-3.03150105849453),
 .UNSPECIFIED.)
CURVE()
GEOMETRIC_REPRESENTATION_ITEM()
RATIONAL_B_SPLINE_CURVE((1.54746358611627,1.66716031106357,1.66716031106357))
REPRESENTATION_ITEM('')
);
#543=(
BOUNDED_CURVE()
B_SPLINE_CURVE(2,(#32607,#32608,#32609),.UNSPECIFIED.,.F.,.F.)
B_SPLINE_CURVE_WITH_KNOTS((3,3),(-3.03150105849453,-1.74744567255227),
 .UNSPECIFIED.)
CURVE()
GEOMETRIC_REPRESENTATION_ITEM()
RATIONAL_B_SPLINE_CURVE((1.66716031106357,1.66716031106357,1.54746358611627))
REPRESENTATION_ITEM('')
);
#544=(
BOUNDED_CURVE()
B_SPLINE_CURVE(2,(#32612,#32613,#32614),.UNSPECIFIED.,.F.,.F.)
B_SPLINE_CURVE_WITH_KNOTS((3,3),(-4.3155564444368,-3.03150105849453),
 .UNSPECIFIED.)
CURVE()
GEOMETRIC_REPRESENTATION_ITEM()
RATIONAL_B_SPLINE_CURVE((1.54746358611627,1.66716031106357,1.66716031106357))
REPRESENTATION_ITEM('')
);
#545=(
BOUNDED_CURVE()
B_SPLINE_CURVE(2,(#32615,#32616,#32617),.UNSPECIFIED.,.F.,.F.)
B_SPLINE_CURVE_WITH_KNOTS((3,3),(-3.03150105849453,-1.74744567255227),
 .UNSPECIFIED.)
CURVE()
GEOMETRIC_REPRESENTATION_ITEM()
RATIONAL_B_SPLINE_CURVE((1.66716031106357,1.66716031106357,1.54746358611627))
REPRESENTATION_ITEM('')
);
#546=(
BOUNDED_CURVE()
B_SPLINE_CURVE(2,(#32620,#32621,#32622),.UNSPECIFIED.,.F.,.F.)
B_SPLINE_CURVE_WITH_KNOTS((3,3),(-3.03150105849454,-1.74744567255227),
 .UNSPECIFIED.)
CURVE()
GEOMETRIC_REPRESENTATION_ITEM()
RATIONAL_B_SPLINE_CURVE((1.66716031106357,1.66716031106357,1.54746358611627))
REPRESENTATION_ITEM('')
);
#547=(
BOUNDED_CURVE()
B_SPLINE_CURVE(2,(#32623,#32624,#32625),.UNSPECIFIED.,.F.,.F.)
B_SPLINE_CURVE_WITH_KNOTS((3,3),(-4.3155564444368,-3.03150105849454),
 .UNSPECIFIED.)
CURVE()
GEOMETRIC_REPRESENTATION_ITEM()
RATIONAL_B_SPLINE_CURVE((1.54746358611627,1.66716031106357,1.66716031106357))
REPRESENTATION_ITEM('')
);
#548=(
BOUNDED_CURVE()
B_SPLINE_CURVE(2,(#32628,#32629,#32630),.UNSPECIFIED.,.F.,.F.)
B_SPLINE_CURVE_WITH_KNOTS((3,3),(-4.3155564444368,-3.03150105849453),
 .UNSPECIFIED.)
CURVE()
GEOMETRIC_REPRESENTATION_ITEM()
RATIONAL_B_SPLINE_CURVE((1.54746358611627,1.66716031106357,1.66716031106357))
REPRESENTATION_ITEM('')
);
#549=(
BOUNDED_CURVE()
B_SPLINE_CURVE(2,(#32631,#32632,#32633),.UNSPECIFIED.,.F.,.F.)
B_SPLINE_CURVE_WITH_KNOTS((3,3),(-3.03150105849454,-1.74744567255227),
 .UNSPECIFIED.)
CURVE()
GEOMETRIC_REPRESENTATION_ITEM()
RATIONAL_B_SPLINE_CURVE((1.66716031106357,1.66716031106357,1.54746358611627))
REPRESENTATION_ITEM('')
);
#618=CONICAL_SURFACE('',#17021,6.8985,0.785398163397446);
#619=CONICAL_SURFACE('',#17040,13.5,1.0471975511966);
#620=CONICAL_SURFACE('',#17041,13.5,1.0471975511966);
#621=CONICAL_SURFACE('',#17042,13.5,1.0471975511966);
#622=CONICAL_SURFACE('',#17043,13.5,1.0471975511966);
#623=CONICAL_SURFACE('',#17044,13.5,1.0471975511966);
#624=CONICAL_SURFACE('',#17045,13.5,1.0471975511966);
#643=TOROIDAL_SURFACE('',#17008,9.2,1.2);
#683=SHAPE_REPRESENTATION_RELATIONSHIP('SRR','None',#33025,#697);
#697=ADVANCED_BREP_SHAPE_REPRESENTATION('',(#1466),#32900);
#1039=CIRCLE('',#17009,8.);
#1040=CIRCLE('',#17010,8.);
#1041=CIRCLE('',#17011,1.2);
#1042=CIRCLE('',#17012,9.2);
#1043=CIRCLE('',#17014,13.5);
#1044=CIRCLE('',#17015,13.5);
#1045=CIRCLE('',#17016,13.5);
#1046=CIRCLE('',#17017,13.5);
#1047=CIRCLE('',#17018,13.5);
#1048=CIRCLE('',#17019,13.5);
#1049=CIRCLE('',#17020,13.5);
#1050=CIRCLE('',#17022,8.);
#1051=CIRCLE('',#17023,6.8985);
#1052=CIRCLE('',#17034,13.5);
#1053=CIRCLE('',#17035,13.5);
#1054=CIRCLE('',#17036,13.5);
#1055=CIRCLE('',#17037,13.5);
#1056=CIRCLE('',#17038,13.5);
#1057=CIRCLE('',#17039,13.5);
#1285=CYLINDRICAL_SURFACE('',#17013,13.5);
#1286=CYLINDRICAL_SURFACE('',#17024,8.);
#1377=STYLED_ITEM('',(#33099),#1466);
#1466=MANIFOLD_SOLID_BREP('Body1',#15625);
#1671=FACE_BOUND('',#3620,.T.);
#2518=FACE_OUTER_BOUND('',#3615,.T.);
#2519=FACE_OUTER_BOUND('',#3616,.T.);
#2520=FACE_OUTER_BOUND('',#3617,.T.);
#2521=FACE_OUTER_BOUND('',#3618,.T.);
#2522=FACE_OUTER_BOUND('',#3619,.T.);
#2523=FACE_OUTER_BOUND('',#3621,.T.);
#2524=FACE_OUTER_BOUND('',#3622,.T.);
#2525=FACE_OUTER_BOUND('',#3623,.T.);
#2526=FACE_OUTER_BOUND('',#3624,.T.);
#2527=FACE_OUTER_BOUND('',#3625,.T.);
#2528=FACE_OUTER_BOUND('',#3626,.T.);
#2529=FACE_OUTER_BOUND('',#3627,.T.);
#2530=FACE_OUTER_BOUND('',#3628,.T.);
#2531=FACE_OUTER_BOUND('',#3629,.T.);
#2532=FACE_OUTER_BOUND('',#3630,.T.);
#2533=FACE_OUTER_BOUND('',#3631,.T.);
#2534=FACE_OUTER_BOUND('',#3632,.T.);
#2535=FACE_OUTER_BOUND('',#3633,.T.);
#2536=FACE_OUTER_BOUND('',#3634,.T.);
#2537=FACE_OUTER_BOUND('',#3635,.T.);
#2538=FACE_OUTER_BOUND('',#3636,.T.);
#2539=FACE_OUTER_BOUND('',#3637,.T.);
#2540=FACE_OUTER_BOUND('',#3638,.T.);
#2541=FACE_OUTER_BOUND('',#3639,.T.);
#2542=FACE_OUTER_BOUND('',#3640,.T.);
#3615=EDGE_LOOP('',(#13825,#13826,#13827,#13828,#13829));
#3616=EDGE_LOOP('',(#13830,#13831,#13832,#13833,#13834,#13835,#13836,#13837,
#13838));
#3617=EDGE_LOOP('',(#13839,#13840,#13841,#13842));
#3618=EDGE_LOOP('',(#13843,#13844,#13845,#13846,#13847));
#3619=EDGE_LOOP('',(#13848));
#3620=EDGE_LOOP('',(#13849));
#3621=EDGE_LOOP('',(#13850));
#3622=EDGE_LOOP('',(#13851,#13852,#13853));
#3623=EDGE_LOOP('',(#13854,#13855,#13856));
#3624=EDGE_LOOP('',(#13857,#13858,#13859));
#3625=EDGE_LOOP('',(#13860,#13861,#13862));
#3626=EDGE_LOOP('',(#13863,#13864,#13865));
#3627=EDGE_LOOP('',(#13866,#13867,#13868));
#3628=EDGE_LOOP('',(#13869,#13870,#13871,#13872,#13873,#13874));
#3629=EDGE_LOOP('',(#13875,#13876,#13877));
#3630=EDGE_LOOP('',(#13878,#13879,#13880));
#3631=EDGE_LOOP('',(#13881,#13882,#13883));
#3632=EDGE_LOOP('',(#13884,#13885,#13886));
#3633=EDGE_LOOP('',(#13887,#13888,#13889));
#3634=EDGE_LOOP('',(#13890,#13891,#13892));
#3635=EDGE_LOOP('',(#13893,#13894,#13895,#13896,#13897,#13898));
#3636=EDGE_LOOP('',(#13899,#13900,#13901,#13902,#13903,#13904));
#3637=EDGE_LOOP('',(#13905,#13906,#13907,#13908,#13909,#13910));
#3638=EDGE_LOOP('',(#13911,#13912,#13913,#13914,#13915,#13916));
#3639=EDGE_LOOP('',(#13917,#13918,#13919,#13920,#13921,#13922));
#3640=EDGE_LOOP('',(#13923,#13924,#13925,#13926,#13927,#13928));
#5044=LINE('',#32532,#6448);
#5045=LINE('',#32543,#6449);
#5046=LINE('',#32546,#6450);
#5047=LINE('',#32551,#6451);
#5048=LINE('',#32552,#6452);
#5049=LINE('',#32555,#6453);
#5050=LINE('',#32556,#6454);
#5051=LINE('',#32559,#6455);
#5052=LINE('',#32560,#6456);
#5053=LINE('',#32563,#6457);
#5054=LINE('',#32564,#6458);
#5055=LINE('',#32567,#6459);
#5056=LINE('',#32568,#6460);
#5057=LINE('',#32571,#6461);
#5058=LINE('',#32572,#6462);
#5059=LINE('',#32635,#6463);
#5060=LINE('',#32636,#6464);
#5061=LINE('',#32638,#6465);
#5062=LINE('',#32640,#6466);
#5063=LINE('',#32642,#6467);
#5064=LINE('',#32644,#6468);
#6448=VECTOR('',#20996,13.5);
#6449=VECTOR('',#21009,6.8985);
#6450=VECTOR('',#21014,8.);
#6451=VECTOR('',#21021,1000.);
#6452=VECTOR('',#21022,1000.);
#6453=VECTOR('',#21025,1000.);
#6454=VECTOR('',#21026,1000.);
#6455=VECTOR('',#21029,1000.);
#6456=VECTOR('',#21030,1000.);
#6457=VECTOR('',#21033,1000.);
#6458=VECTOR('',#21034,1000.);
#6459=VECTOR('',#21037,1000.);
#6460=VECTOR('',#21038,1000.);
#6461=VECTOR('',#21041,1000.);
#6462=VECTOR('',#21042,1000.);
#6463=VECTOR('',#21071,1000.);
#6464=VECTOR('',#21072,1000.);
#6465=VECTOR('',#21075,1000.);
#6466=VECTOR('',#21078,1000.);
#6467=VECTOR('',#21081,1000.);
#6468=VECTOR('',#21084,1000.);
#7772=VERTEX_POINT('',#32516);
#7773=VERTEX_POINT('',#32517);
#7774=VERTEX_POINT('',#32520);
#7775=VERTEX_POINT('',#32524);
#7776=VERTEX_POINT('',#32525);
#7777=VERTEX_POINT('',#32527);
#7778=VERTEX_POINT('',#32529);
#7779=VERTEX_POINT('',#32531);
#7780=VERTEX_POINT('',#32534);
#7781=VERTEX_POINT('',#32536);
#7782=VERTEX_POINT('',#32540);
#7783=VERTEX_POINT('',#32542);
#7784=VERTEX_POINT('',#32550);
#7785=VERTEX_POINT('',#32554);
#7786=VERTEX_POINT('',#32558);
#7787=VERTEX_POINT('',#32562);
#7788=VERTEX_POINT('',#32566);
#7789=VERTEX_POINT('',#32570);
#7790=VERTEX_POINT('',#32574);
#7791=VERTEX_POINT('',#32575);
#7792=VERTEX_POINT('',#32577);
#7793=VERTEX_POINT('',#32579);
#7794=VERTEX_POINT('',#32581);
#7795=VERTEX_POINT('',#32583);
#7796=VERTEX_POINT('',#32587);
#7797=VERTEX_POINT('',#32595);
#7798=VERTEX_POINT('',#32603);
#7799=VERTEX_POINT('',#32611);
#7800=VERTEX_POINT('',#32619);
#7801=VERTEX_POINT('',#32627);
#9796=EDGE_CURVE('',#7772,#7773,#1039,.T.);
#9797=EDGE_CURVE('',#7773,#7772,#1040,.T.);
#9798=EDGE_CURVE('',#7773,#7774,#1041,.T.);
#9799=EDGE_CURVE('',#7774,#7774,#1042,.T.);
#9800=EDGE_CURVE('',#7775,#7776,#1043,.T.);
#9801=EDGE_CURVE('',#7777,#7775,#1044,.T.);
#9802=EDGE_CURVE('',#7778,#7777,#1045,.T.);
#9803=EDGE_CURVE('',#7778,#7779,#5044,.T.);
#9804=EDGE_CURVE('',#7779,#7779,#1046,.T.);
#9805=EDGE_CURVE('',#7780,#7778,#1047,.T.);
#9806=EDGE_CURVE('',#7781,#7780,#1048,.T.);
#9807=EDGE_CURVE('',#7776,#7781,#1049,.T.);
#9808=EDGE_CURVE('',#7782,#7782,#1050,.T.);
#9809=EDGE_CURVE('',#7782,#7783,#5045,.T.);
#9810=EDGE_CURVE('',#7783,#7783,#1051,.T.);
#9811=EDGE_CURVE('',#7772,#7782,#5046,.T.);
#9812=EDGE_CURVE('',#7784,#7780,#5047,.T.);
#9813=EDGE_CURVE('',#7778,#7784,#5048,.T.);
#9814=EDGE_CURVE('',#7780,#7785,#5049,.T.);
#9815=EDGE_CURVE('',#7785,#7781,#5050,.T.);
#9816=EDGE_CURVE('',#7781,#7786,#5051,.T.);
#9817=EDGE_CURVE('',#7786,#7776,#5052,.T.);
#9818=EDGE_CURVE('',#7776,#7787,#5053,.T.);
#9819=EDGE_CURVE('',#7787,#7775,#5054,.T.);
#9820=EDGE_CURVE('',#7775,#7788,#5055,.T.);
#9821=EDGE_CURVE('',#7788,#7777,#5056,.T.);
#9822=EDGE_CURVE('',#7777,#7789,#5057,.T.);
#9823=EDGE_CURVE('',#7789,#7778,#5058,.T.);
#9824=EDGE_CURVE('',#7790,#7791,#1052,.T.);
#9825=EDGE_CURVE('',#7792,#7790,#1053,.T.);
#9826=EDGE_CURVE('',#7793,#7792,#1054,.T.);
#9827=EDGE_CURVE('',#7794,#7793,#1055,.T.);
#9828=EDGE_CURVE('',#7794,#7795,#1056,.T.);
#9829=EDGE_CURVE('',#7791,#7795,#1057,.T.);
#9830=EDGE_CURVE('',#7795,#7796,#538,.T.);
#9831=EDGE_CURVE('',#7796,#7791,#539,.T.);
#9832=EDGE_CURVE('',#7794,#7797,#540,.T.);
#9833=EDGE_CURVE('',#7797,#7795,#541,.T.);
#9834=EDGE_CURVE('',#7798,#7794,#542,.T.);
#9835=EDGE_CURVE('',#7793,#7798,#543,.T.);
#9836=EDGE_CURVE('',#7799,#7793,#544,.T.);
#9837=EDGE_CURVE('',#7792,#7799,#545,.T.);
#9838=EDGE_CURVE('',#7791,#7800,#546,.T.);
#9839=EDGE_CURVE('',#7800,#7790,#547,.T.);
#9840=EDGE_CURVE('',#7801,#7792,#548,.T.);
#9841=EDGE_CURVE('',#7790,#7801,#549,.T.);
#9842=EDGE_CURVE('',#7789,#7801,#5059,.T.);
#9843=EDGE_CURVE('',#7784,#7800,#5060,.T.);
#9844=EDGE_CURVE('',#7788,#7799,#5061,.T.);
#9845=EDGE_CURVE('',#7787,#7798,#5062,.T.);
#9846=EDGE_CURVE('',#7786,#7797,#5063,.T.);
#9847=EDGE_CURVE('',#7785,#7796,#5064,.T.);
#13825=ORIENTED_EDGE('',*,*,#9796,.F.);
#13826=ORIENTED_EDGE('',*,*,#9797,.F.);
#13827=ORIENTED_EDGE('',*,*,#9798,.T.);
#13828=ORIENTED_EDGE('',*,*,#9799,.F.);
#13829=ORIENTED_EDGE('',*,*,#9798,.F.);
#13830=ORIENTED_EDGE('',*,*,#9800,.F.);
#13831=ORIENTED_EDGE('',*,*,#9801,.F.);
#13832=ORIENTED_EDGE('',*,*,#9802,.F.);
#13833=ORIENTED_EDGE('',*,*,#9803,.T.);
#13834=ORIENTED_EDGE('',*,*,#9804,.F.);
#13835=ORIENTED_EDGE('',*,*,#9803,.F.);
#13836=ORIENTED_EDGE('',*,*,#9805,.F.);
#13837=ORIENTED_EDGE('',*,*,#9806,.F.);
#13838=ORIENTED_EDGE('',*,*,#9807,.F.);
#13839=ORIENTED_EDGE('',*,*,#9808,.F.);
#13840=ORIENTED_EDGE('',*,*,#9809,.T.);
#13841=ORIENTED_EDGE('',*,*,#9810,.T.);
#13842=ORIENTED_EDGE('',*,*,#9809,.F.);
#13843=ORIENTED_EDGE('',*,*,#9796,.T.);
#13844=ORIENTED_EDGE('',*,*,#9797,.T.);
#13845=ORIENTED_EDGE('',*,*,#9811,.T.);
#13846=ORIENTED_EDGE('',*,*,#9808,.T.);
#13847=ORIENTED_EDGE('',*,*,#9811,.F.);
#13848=ORIENTED_EDGE('',*,*,#9804,.T.);
#13849=ORIENTED_EDGE('',*,*,#9799,.T.);
#13850=ORIENTED_EDGE('',*,*,#9810,.F.);
#13851=ORIENTED_EDGE('',*,*,#9812,.T.);
#13852=ORIENTED_EDGE('',*,*,#9805,.T.);
#13853=ORIENTED_EDGE('',*,*,#9813,.T.);
#13854=ORIENTED_EDGE('',*,*,#9814,.T.);
#13855=ORIENTED_EDGE('',*,*,#9815,.T.);
#13856=ORIENTED_EDGE('',*,*,#9806,.T.);
#13857=ORIENTED_EDGE('',*,*,#9816,.T.);
#13858=ORIENTED_EDGE('',*,*,#9817,.T.);
#13859=ORIENTED_EDGE('',*,*,#9807,.T.);
#13860=ORIENTED_EDGE('',*,*,#9818,.T.);
#13861=ORIENTED_EDGE('',*,*,#9819,.T.);
#13862=ORIENTED_EDGE('',*,*,#9800,.T.);
#13863=ORIENTED_EDGE('',*,*,#9820,.T.);
#13864=ORIENTED_EDGE('',*,*,#9821,.T.);
#13865=ORIENTED_EDGE('',*,*,#9801,.T.);
#13866=ORIENTED_EDGE('',*,*,#9822,.T.);
#13867=ORIENTED_EDGE('',*,*,#9823,.T.);
#13868=ORIENTED_EDGE('',*,*,#9802,.T.);
#13869=ORIENTED_EDGE('',*,*,#9824,.F.);
#13870=ORIENTED_EDGE('',*,*,#9825,.F.);
#13871=ORIENTED_EDGE('',*,*,#9826,.F.);
#13872=ORIENTED_EDGE('',*,*,#9827,.F.);
#13873=ORIENTED_EDGE('',*,*,#9828,.T.);
#13874=ORIENTED_EDGE('',*,*,#9829,.F.);
#13875=ORIENTED_EDGE('',*,*,#9830,.T.);
#13876=ORIENTED_EDGE('',*,*,#9831,.T.);
#13877=ORIENTED_EDGE('',*,*,#9829,.T.);
#13878=ORIENTED_EDGE('',*,*,#9832,.T.);
#13879=ORIENTED_EDGE('',*,*,#9833,.T.);
#13880=ORIENTED_EDGE('',*,*,#9828,.F.);
#13881=ORIENTED_EDGE('',*,*,#9834,.T.);
#13882=ORIENTED_EDGE('',*,*,#9827,.T.);
#13883=ORIENTED_EDGE('',*,*,#9835,.T.);
#13884=ORIENTED_EDGE('',*,*,#9836,.T.);
#13885=ORIENTED_EDGE('',*,*,#9826,.T.);
#13886=ORIENTED_EDGE('',*,*,#9837,.T.);
#13887=ORIENTED_EDGE('',*,*,#9838,.T.);
#13888=ORIENTED_EDGE('',*,*,#9839,.T.);
#13889=ORIENTED_EDGE('',*,*,#9824,.T.);
#13890=ORIENTED_EDGE('',*,*,#9840,.T.);
#13891=ORIENTED_EDGE('',*,*,#9825,.T.);
#13892=ORIENTED_EDGE('',*,*,#9841,.T.);
#13893=ORIENTED_EDGE('',*,*,#9823,.F.);
#13894=ORIENTED_EDGE('',*,*,#9842,.T.);
#13895=ORIENTED_EDGE('',*,*,#9841,.F.);
#13896=ORIENTED_EDGE('',*,*,#9839,.F.);
#13897=ORIENTED_EDGE('',*,*,#9843,.F.);
#13898=ORIENTED_EDGE('',*,*,#9813,.F.);
#13899=ORIENTED_EDGE('',*,*,#9821,.F.);
#13900=ORIENTED_EDGE('',*,*,#9844,.T.);
#13901=ORIENTED_EDGE('',*,*,#9837,.F.);
#13902=ORIENTED_EDGE('',*,*,#9840,.F.);
#13903=ORIENTED_EDGE('',*,*,#9842,.F.);
#13904=ORIENTED_EDGE('',*,*,#9822,.F.);
#13905=ORIENTED_EDGE('',*,*,#9819,.F.);
#13906=ORIENTED_EDGE('',*,*,#9845,.T.);
#13907=ORIENTED_EDGE('',*,*,#9835,.F.);
#13908=ORIENTED_EDGE('',*,*,#9836,.F.);
#13909=ORIENTED_EDGE('',*,*,#9844,.F.);
#13910=ORIENTED_EDGE('',*,*,#9820,.F.);
#13911=ORIENTED_EDGE('',*,*,#9817,.F.);
#13912=ORIENTED_EDGE('',*,*,#9846,.T.);
#13913=ORIENTED_EDGE('',*,*,#9832,.F.);
#13914=ORIENTED_EDGE('',*,*,#9834,.F.);
#13915=ORIENTED_EDGE('',*,*,#9845,.F.);
#13916=ORIENTED_EDGE('',*,*,#9818,.F.);
#13917=ORIENTED_EDGE('',*,*,#9815,.F.);
#13918=ORIENTED_EDGE('',*,*,#9847,.T.);
#13919=ORIENTED_EDGE('',*,*,#9830,.F.);
#13920=ORIENTED_EDGE('',*,*,#9833,.F.);
#13921=ORIENTED_EDGE('',*,*,#9846,.F.);
#13922=ORIENTED_EDGE('',*,*,#9816,.F.);
#13923=ORIENTED_EDGE('',*,*,#9812,.F.);
#13924=ORIENTED_EDGE('',*,*,#9843,.T.);
#13925=ORIENTED_EDGE('',*,*,#9838,.F.);
#13926=ORIENTED_EDGE('',*,*,#9831,.F.);
#13927=ORIENTED_EDGE('',*,*,#9847,.F.);
#13928=ORIENTED_EDGE('',*,*,#9814,.F.);
#14619=PLANE('',#17025);
#14620=PLANE('',#17026);
#14621=PLANE('',#17027);
#14622=PLANE('',#17028);
#14623=PLANE('',#17029);
#14624=PLANE('',#17030);
#14625=PLANE('',#17031);
#14626=PLANE('',#17032);
#14627=PLANE('',#17033);
#14628=PLANE('',#17046);
#14629=PLANE('',#17047);
#14630=PLANE('',#17048);
#14631=PLANE('',#17049);
#14632=PLANE('',#17050);
#14633=PLANE('',#17051);
#15486=ADVANCED_FACE('',(#2518),#643,.F.);
#15487=ADVANCED_FACE('',(#2519),#1285,.T.);
#15488=ADVANCED_FACE('',(#2520),#618,.T.);
#15489=ADVANCED_FACE('',(#2521),#1286,.T.);
#15490=ADVANCED_FACE('',(#2522,#1671),#14619,.T.);
#15491=ADVANCED_FACE('',(#2523),#14620,.F.);
#15492=ADVANCED_FACE('',(#2524),#14621,.T.);
#15493=ADVANCED_FACE('',(#2525),#14622,.T.);
#15494=ADVANCED_FACE('',(#2526),#14623,.T.);
#15495=ADVANCED_FACE('',(#2527),#14624,.T.);
#15496=ADVANCED_FACE('',(#2528),#14625,.T.);
#15497=ADVANCED_FACE('',(#2529),#14626,.T.);
#15498=ADVANCED_FACE('',(#2530),#14627,.F.);
#15499=ADVANCED_FACE('',(#2531),#619,.T.);
#15500=ADVANCED_FACE('',(#2532),#620,.T.);
#15501=ADVANCED_FACE('',(#2533),#621,.T.);
#15502=ADVANCED_FACE('',(#2534),#622,.T.);
#15503=ADVANCED_FACE('',(#2535),#623,.T.);
#15504=ADVANCED_FACE('',(#2536),#624,.T.);
#15505=ADVANCED_FACE('',(#2537),#14628,.F.);
#15506=ADVANCED_FACE('',(#2538),#14629,.F.);
#15507=ADVANCED_FACE('',(#2539),#14630,.F.);
#15508=ADVANCED_FACE('',(#2540),#14631,.F.);
#15509=ADVANCED_FACE('',(#2541),#14632,.F.);
#15510=ADVANCED_FACE('',(#2542),#14633,.F.);
#15625=CLOSED_SHELL('',(#15486,#15487,#15488,#15489,#15490,#15491,#15492,
#15493,#15494,#15495,#15496,#15497,#15498,#15499,#15500,#15501,#15502,#15503,
#15504,#15505,#15506,#15507,#15508,#15509,#15510));
#17007=AXIS2_PLACEMENT_3D('',#32514,#20976,#20977);
#17008=AXIS2_PLACEMENT_3D('',#32515,#20978,#20979);
#17009=AXIS2_PLACEMENT_3D('',#32518,#20980,#20981);
#17010=AXIS2_PLACEMENT_3D('',#32519,#20982,#20983);
#17011=AXIS2_PLACEMENT_3D('',#32521,#20984,#20985);
#17012=AXIS2_PLACEMENT_3D('',#32522,#20986,#20987);
#17013=AXIS2_PLACEMENT_3D('',#32523,#20988,#20989);
#17014=AXIS2_PLACEMENT_3D('',#32526,#20990,#20991);
#17015=AXIS2_PLACEMENT_3D('',#32528,#20992,#20993);
#17016=AXIS2_PLACEMENT_3D('',#32530,#20994,#20995);
#17017=AXIS2_PLACEMENT_3D('',#32533,#20997,#20998);
#17018=AXIS2_PLACEMENT_3D('',#32535,#20999,#21000);
#17019=AXIS2_PLACEMENT_3D('',#32537,#21001,#21002);
#17020=AXIS2_PLACEMENT_3D('',#32538,#21003,#21004);
#17021=AXIS2_PLACEMENT_3D('',#32539,#21005,#21006);
#17022=AXIS2_PLACEMENT_3D('',#32541,#21007,#21008);
#17023=AXIS2_PLACEMENT_3D('',#32544,#21010,#21011);
#17024=AXIS2_PLACEMENT_3D('',#32545,#21012,#21013);
#17025=AXIS2_PLACEMENT_3D('',#32547,#21015,#21016);
#17026=AXIS2_PLACEMENT_3D('',#32548,#21017,#21018);
#17027=AXIS2_PLACEMENT_3D('',#32549,#21019,#21020);
#17028=AXIS2_PLACEMENT_3D('',#32553,#21023,#21024);
#17029=AXIS2_PLACEMENT_3D('',#32557,#21027,#21028);
#17030=AXIS2_PLACEMENT_3D('',#32561,#21031,#21032);
#17031=AXIS2_PLACEMENT_3D('',#32565,#21035,#21036);
#17032=AXIS2_PLACEMENT_3D('',#32569,#21039,#21040);
#17033=AXIS2_PLACEMENT_3D('',#32573,#21043,#21044);
#17034=AXIS2_PLACEMENT_3D('',#32576,#21045,#21046);
#17035=AXIS2_PLACEMENT_3D('',#32578,#21047,#21048);
#17036=AXIS2_PLACEMENT_3D('',#32580,#21049,#21050);
#17037=AXIS2_PLACEMENT_3D('',#32582,#21051,#21052);
#17038=AXIS2_PLACEMENT_3D('',#32584,#21053,#21054);
#17039=AXIS2_PLACEMENT_3D('',#32585,#21055,#21056);
#17040=AXIS2_PLACEMENT_3D('',#32586,#21057,#21058);
#17041=AXIS2_PLACEMENT_3D('',#32594,#21059,#21060);
#17042=AXIS2_PLACEMENT_3D('',#32602,#21061,#21062);
#17043=AXIS2_PLACEMENT_3D('',#32610,#21063,#21064);
#17044=AXIS2_PLACEMENT_3D('',#32618,#21065,#21066);
#17045=AXIS2_PLACEMENT_3D('',#32626,#21067,#21068);
#17046=AXIS2_PLACEMENT_3D('',#32634,#21069,#21070);
#17047=AXIS2_PLACEMENT_3D('',#32637,#21073,#21074);
#17048=AXIS2_PLACEMENT_3D('',#32639,#21076,#21077);
#17049=AXIS2_PLACEMENT_3D('',#32641,#21079,#21080);
#17050=AXIS2_PLACEMENT_3D('',#32643,#21082,#21083);
#17051=AXIS2_PLACEMENT_3D('',#32645,#21085,#21086);
#20976=DIRECTION('axis',(0.,0.,1.));
#20977=DIRECTION('refdir',(1.,0.,0.));
#20978=DIRECTION('center_axis',(1.,0.,0.));
#20979=DIRECTION('ref_axis',(0.,0.,-1.));
#20980=DIRECTION('center_axis',(1.,0.,0.));
#20981=DIRECTION('ref_axis',(0.,0.,-1.));
#20982=DIRECTION('center_axis',(1.,0.,0.));
#20983=DIRECTION('ref_axis',(0.,0.,-1.));
#20984=DIRECTION('center_axis',(0.,1.,1.22464679914735E-16));
#20985=DIRECTION('ref_axis',(0.,-1.22464679914735E-16,1.));
#20986=DIRECTION('center_axis',(-1.,0.,0.));
#20987=DIRECTION('ref_axis',(0.,0.,-1.));
#20988=DIRECTION('center_axis',(-1.,0.,0.));
#20989=DIRECTION('ref_axis',(0.,0.,1.));
#20990=DIRECTION('center_axis',(-1.,0.,0.));
#20991=DIRECTION('ref_axis',(0.,0.,1.));
#20992=DIRECTION('center_axis',(-1.,0.,0.));
#20993=DIRECTION('ref_axis',(0.,0.,1.));
#20994=DIRECTION('center_axis',(-1.,0.,0.));
#20995=DIRECTION('ref_axis',(0.,0.,1.));
#20996=DIRECTION('',(1.,0.,0.));
#20997=DIRECTION('center_axis',(1.,0.,0.));
#20998=DIRECTION('ref_axis',(0.,0.,-1.));
#20999=DIRECTION('center_axis',(-1.,0.,0.));
#21000=DIRECTION('ref_axis',(0.,0.,1.));
#21001=DIRECTION('center_axis',(-1.,0.,0.));
#21002=DIRECTION('ref_axis',(0.,0.,1.));
#21003=DIRECTION('center_axis',(-1.,0.,0.));
#21004=DIRECTION('ref_axis',(0.,0.,1.));
#21005=DIRECTION('center_axis',(-1.,0.,0.));
#21006=DIRECTION('ref_axis',(0.,0.,1.));
#21007=DIRECTION('center_axis',(-1.,0.,0.));
#21008=DIRECTION('ref_axis',(0.,0.,1.));
#21009=DIRECTION('',(0.707106781186549,8.65956056235491E-17,0.707106781186546));
#21010=DIRECTION('center_axis',(-1.,0.,0.));
#21011=DIRECTION('ref_axis',(0.,0.,1.));
#21012=DIRECTION('center_axis',(-1.,0.,0.));
#21013=DIRECTION('ref_axis',(0.,0.,1.));
#21014=DIRECTION('',(1.,0.,0.));
#21015=DIRECTION('center_axis',(1.,0.,0.));
#21016=DIRECTION('ref_axis',(0.,0.,-1.));
#21017=DIRECTION('center_axis',(-1.,0.,0.));
#21018=DIRECTION('ref_axis',(0.,0.,1.));
#21019=DIRECTION('center_axis',(1.,0.,0.));
#21020=DIRECTION('ref_axis',(0.,0.,-1.));
#21021=DIRECTION('',(0.,0.500000000000001,0.866025403784438));
#21022=DIRECTION('',(0.,1.,2.22565125738838E-16));
#21023=DIRECTION('center_axis',(1.,0.,0.));
#21024=DIRECTION('ref_axis',(0.,0.,-1.));
#21025=DIRECTION('',(0.,0.500000000000001,0.866025403784438));
#21026=DIRECTION('',(0.,-0.500000000000001,0.866025403784438));
#21027=DIRECTION('center_axis',(1.,0.,0.));
#21028=DIRECTION('ref_axis',(0.,0.,-1.));
#21029=DIRECTION('',(0.,-0.500000000000001,0.866025403784438));
#21030=DIRECTION('',(0.,-1.,2.22565125738839E-16));
#21031=DIRECTION('center_axis',(1.,0.,0.));
#21032=DIRECTION('ref_axis',(0.,0.,-1.));
#21033=DIRECTION('',(0.,-1.,2.22565125738839E-16));
#21034=DIRECTION('',(0.,-0.500000000000001,-0.866025403784438));
#21035=DIRECTION('center_axis',(1.,0.,0.));
#21036=DIRECTION('ref_axis',(0.,0.,-1.));
#21037=DIRECTION('',(0.,-0.500000000000001,-0.866025403784438));
#21038=DIRECTION('',(0.,0.5,-0.866025403784439));
#21039=DIRECTION('center_axis',(1.,0.,0.));
#21040=DIRECTION('ref_axis',(0.,0.,-1.));
#21041=DIRECTION('',(0.,0.5,-0.866025403784439));
#21042=DIRECTION('',(0.,1.,2.22565125738838E-16));
#21043=DIRECTION('center_axis',(1.,0.,0.));
#21044=DIRECTION('ref_axis',(0.,0.,-1.));
#21045=DIRECTION('center_axis',(1.,0.,0.));
#21046=DIRECTION('ref_axis',(0.,0.,-1.));
#21047=DIRECTION('center_axis',(1.,0.,0.));
#21048=DIRECTION('ref_axis',(0.,0.,-1.));
#21049=DIRECTION('center_axis',(1.,0.,0.));
#21050=DIRECTION('ref_axis',(0.,0.,-1.));
#21051=DIRECTION('center_axis',(1.,0.,0.));
#21052=DIRECTION('ref_axis',(0.,0.,-1.));
#21053=DIRECTION('center_axis',(-1.,0.,0.));
#21054=DIRECTION('ref_axis',(0.,0.,1.));
#21055=DIRECTION('center_axis',(1.,0.,0.));
#21056=DIRECTION('ref_axis',(0.,0.,-1.));
#21057=DIRECTION('center_axis',(1.,0.,0.));
#21058=DIRECTION('ref_axis',(0.,0.,-1.));
#21059=DIRECTION('center_axis',(1.,0.,0.));
#21060=DIRECTION('ref_axis',(0.,0.,-1.));
#21061=DIRECTION('center_axis',(1.,0.,0.));
#21062=DIRECTION('ref_axis',(0.,0.,-1.));
#21063=DIRECTION('center_axis',(1.,0.,0.));
#21064=DIRECTION('ref_axis',(0.,0.,-1.));
#21065=DIRECTION('center_axis',(1.,0.,0.));
#21066=DIRECTION('ref_axis',(0.,0.,-1.));
#21067=DIRECTION('center_axis',(1.,0.,0.));
#21068=DIRECTION('ref_axis',(0.,0.,-1.));
#21069=DIRECTION('center_axis',(0.,-2.22565125738838E-16,1.));
#21070=DIRECTION('ref_axis',(0.,-1.,-2.22565125738838E-16));
#21071=DIRECTION('',(-1.,0.,0.));
#21072=DIRECTION('',(-1.,0.,0.));
#21073=DIRECTION('center_axis',(0.,0.866025403784439,0.5));
#21074=DIRECTION('ref_axis',(0.,-0.5,0.866025403784439));
#21075=DIRECTION('',(-1.,0.,0.));
#21076=DIRECTION('center_axis',(0.,0.866025403784438,-0.500000000000001));
#21077=DIRECTION('ref_axis',(0.,0.500000000000001,0.866025403784438));
#21078=DIRECTION('',(-1.,0.,0.));
#21079=DIRECTION('center_axis',(0.,-2.22565125738839E-16,-1.));
#21080=DIRECTION('ref_axis',(0.,1.,-2.22565125738839E-16));
#21081=DIRECTION('',(-1.,0.,0.));
#21082=DIRECTION('center_axis',(0.,-0.866025403784438,-0.500000000000001));
#21083=DIRECTION('ref_axis',(0.,0.500000000000001,-0.866025403784438));
#21084=DIRECTION('',(-1.,0.,0.));
#21085=DIRECTION('center_axis',(0.,-0.866025403784438,0.500000000000001));
#21086=DIRECTION('ref_axis',(0.,-0.500000000000001,-0.866025403784438));
#32514=CARTESIAN_POINT('',(0.,0.,0.));
#32515=CARTESIAN_POINT('Origin',(11.2,0.,0.));
#32516=CARTESIAN_POINT('',(11.2,9.79717439317883E-16,-8.));
#32517=CARTESIAN_POINT('',(11.2,-9.79717439317883E-16,8.));
#32518=CARTESIAN_POINT('Origin',(11.2,0.,0.));
#32519=CARTESIAN_POINT('Origin',(11.2,0.,0.));
#32520=CARTESIAN_POINT('',(10.,-1.12667505521557E-15,9.2));
#32521=CARTESIAN_POINT('Origin',(11.2,-1.12667505521557E-15,9.2));
#32522=CARTESIAN_POINT('Origin',(10.,0.,0.));
#32523=CARTESIAN_POINT('Origin',(0.,0.,0.));
#32524=CARTESIAN_POINT('',(9.4,-11.6913429510899,6.75000000000002));
#32525=CARTESIAN_POINT('',(9.4,0.,13.5));
#32526=CARTESIAN_POINT('Origin',(9.4,0.,0.));
#32527=CARTESIAN_POINT('',(9.4,-11.6913429510899,-6.75));
#32528=CARTESIAN_POINT('Origin',(9.4,0.,0.));
#32529=CARTESIAN_POINT('',(9.4,3.00462919747432E-15,-13.5));
#32530=CARTESIAN_POINT('Origin',(9.4,0.,0.));
#32531=CARTESIAN_POINT('',(10.,-1.65327317884893E-15,-13.5));
#32532=CARTESIAN_POINT('',(0.,-1.65327317884893E-15,-13.5));
#32533=CARTESIAN_POINT('Origin',(10.,0.,0.));
#32534=CARTESIAN_POINT('',(9.4,11.6913429510899,-6.75000000000001));
#32535=CARTESIAN_POINT('Origin',(9.4,0.,0.));
#32536=CARTESIAN_POINT('',(9.4,11.6913429510899,6.75000000000001));
#32537=CARTESIAN_POINT('Origin',(9.4,0.,0.));
#32538=CARTESIAN_POINT('Origin',(9.4,0.,0.));
#32539=CARTESIAN_POINT('Origin',(70.,0.,0.));
#32540=CARTESIAN_POINT('',(68.8985,-9.79717439317882E-16,-8.));
#32541=CARTESIAN_POINT('Origin',(68.8985,0.,0.));
#32542=CARTESIAN_POINT('',(70.,-8.44822594391802E-16,-6.8985));
#32543=CARTESIAN_POINT('',(70.,-8.44822594391802E-16,-6.8985));
#32544=CARTESIAN_POINT('Origin',(70.,0.,0.));
#32545=CARTESIAN_POINT('Origin',(0.,0.,0.));
#32546=CARTESIAN_POINT('',(0.,-9.79717439317883E-16,-8.));
#32547=CARTESIAN_POINT('Origin',(10.,15.5884572681199,-1.3010426069826E-15));
#32548=CARTESIAN_POINT('Origin',(70.,0.,0.));
#32549=CARTESIAN_POINT('Origin',(9.4,13.5,0.));
#32550=CARTESIAN_POINT('',(9.4,7.79422863405994,-13.5));
#32551=CARTESIAN_POINT('',(9.4,7.79422863405994,-13.5));
#32552=CARTESIAN_POINT('',(9.4,7.79422863405994,-13.5));
#32553=CARTESIAN_POINT('Origin',(9.4,13.5,0.));
#32554=CARTESIAN_POINT('',(9.4,15.5884572681199,0.));
#32555=CARTESIAN_POINT('',(9.4,7.79422863405994,-13.5));
#32556=CARTESIAN_POINT('',(9.4,15.5884572681199,0.));
#32557=CARTESIAN_POINT('Origin',(9.4,13.5,0.));
#32558=CARTESIAN_POINT('',(9.4,7.79422863405994,13.5));
#32559=CARTESIAN_POINT('',(9.4,15.5884572681199,0.));
#32560=CARTESIAN_POINT('',(9.4,7.79422863405994,13.5));
#32561=CARTESIAN_POINT('Origin',(9.4,13.5,0.));
#32562=CARTESIAN_POINT('',(9.4,-7.79422863405994,13.5));
#32563=CARTESIAN_POINT('',(9.4,7.79422863405994,13.5));
#32564=CARTESIAN_POINT('',(9.4,-15.5884572681199,8.77615707241165E-17));
#32565=CARTESIAN_POINT('Origin',(9.4,13.5,0.));
#32566=CARTESIAN_POINT('',(9.4,-15.5884572681199,0.));
#32567=CARTESIAN_POINT('',(9.4,-15.5884572681199,8.77615707241165E-17));
#32568=CARTESIAN_POINT('',(9.4,-7.79422863405996,-13.5));
#32569=CARTESIAN_POINT('Origin',(9.4,13.5,0.));
#32570=CARTESIAN_POINT('',(9.4,-7.79422863405996,-13.5));
#32571=CARTESIAN_POINT('',(9.4,-7.79422863405996,-13.5));
#32572=CARTESIAN_POINT('',(9.4,7.79422863405994,-13.5));
#32573=CARTESIAN_POINT('Origin',(0.,15.5884572681199,-1.3010426069826E-15));
#32574=CARTESIAN_POINT('',(0.,3.00462919747432E-15,-13.5));
#32575=CARTESIAN_POINT('',(0.,11.6913429510899,-6.75000000000001));
#32576=CARTESIAN_POINT('Origin',(0.,0.,0.));
#32577=CARTESIAN_POINT('',(0.,-11.6913429510899,-6.75));
#32578=CARTESIAN_POINT('Origin',(0.,0.,0.));
#32579=CARTESIAN_POINT('',(0.,-11.6913429510899,6.75000000000001));
#32580=CARTESIAN_POINT('Origin',(0.,0.,0.));
#32581=CARTESIAN_POINT('',(0.,3.00462919747432E-15,13.5));
#32582=CARTESIAN_POINT('Origin',(0.,0.,0.));
#32583=CARTESIAN_POINT('',(0.,11.6913429510899,6.75000000000001));
#32584=CARTESIAN_POINT('Origin',(0.,0.,0.));
#32585=CARTESIAN_POINT('Origin',(0.,0.,0.));
#32586=CARTESIAN_POINT('Origin',(0.,0.,0.));
#32587=CARTESIAN_POINT('',(1.20577136594005,15.5884572681199,1.14068201043699E-16));
#32588=CARTESIAN_POINT('Ctrl Pts',(7.99123887912295E-16,11.6913429510899,
6.75000000000001));
#32589=CARTESIAN_POINT('Ctrl Pts',(2.44249065417534E-15,13.5000000000004,
3.61731409781943));
#32590=CARTESIAN_POINT('Ctrl Pts',(1.20577136594065,15.5884572681209,-1.81141005043525E-12));
#32591=CARTESIAN_POINT('Ctrl Pts',(1.20577136594066,15.588457268121,1.8228892015787E-12));
#32592=CARTESIAN_POINT('Ctrl Pts',(3.6583932433027E-15,13.5000000000004,
-3.61731409781942));
#32593=CARTESIAN_POINT('Ctrl Pts',(7.99123887912298E-16,11.6913429510899,
-6.75));
#32594=CARTESIAN_POINT('Origin',(0.,0.,0.));
#32595=CARTESIAN_POINT('',(1.20577136594004,7.79422863405994,13.5));
#32596=CARTESIAN_POINT('Ctrl Pts',(2.66374629304099E-16,-1.06549851721639E-15,
13.5));
#32597=CARTESIAN_POINT('Ctrl Pts',(-6.66133814775094E-16,3.617314097821,
13.5));
#32598=CARTESIAN_POINT('Ctrl Pts',(1.20577136594065,7.79422863406204,13.5));
#32599=CARTESIAN_POINT('Ctrl Pts',(1.20577136594064,7.7942286340589,13.5000000000018));
#32600=CARTESIAN_POINT('Ctrl Pts',(-6.67981053492038E-16,9.88268590217942,
9.88268590218058));
#32601=CARTESIAN_POINT('Ctrl Pts',(7.99123887912295E-16,11.6913429510899,
6.75000000000001));
#32602=CARTESIAN_POINT('Origin',(0.,0.,0.));
#32603=CARTESIAN_POINT('',(1.20577136594004,-7.79422863405994,13.5));
#32604=CARTESIAN_POINT('Ctrl Pts',(1.20577136594065,-7.79422863406204,13.5));
#32605=CARTESIAN_POINT('Ctrl Pts',(1.09406226090395E-15,-3.617314097821,
13.5));
#32606=CARTESIAN_POINT('Ctrl Pts',(2.66374629304099E-16,-1.06549851721639E-15,
13.5));
#32607=CARTESIAN_POINT('Ctrl Pts',(3.19649555164917E-15,-11.6913429510899,
6.75000000000002));
#32608=CARTESIAN_POINT('Ctrl Pts',(3.44169137633799E-15,-9.88268590217941,
9.88268590218058));
#32609=CARTESIAN_POINT('Ctrl Pts',(1.20577136594065,-7.79422863405889,13.5000000000018));
#32610=CARTESIAN_POINT('Origin',(0.,0.,0.));
#32611=CARTESIAN_POINT('',(1.20577136594005,-15.5884572681199,1.05679326596683E-16));
#32612=CARTESIAN_POINT('Ctrl Pts',(1.20577136594066,-15.588457268121,-1.82403711669304E-12));
#32613=CARTESIAN_POINT('Ctrl Pts',(3.15927592518995E-15,-13.5000000000004,
3.61731409781943));
#32614=CARTESIAN_POINT('Ctrl Pts',(3.19649555164917E-15,-11.6913429510899,
6.75000000000002));
#32615=CARTESIAN_POINT('Ctrl Pts',(5.59386721538605E-15,-11.6913429510899,
-6.75000000000001));
#32616=CARTESIAN_POINT('Ctrl Pts',(4.77395900588817E-15,-13.5000000000004,
-3.61731409781943));
#32617=CARTESIAN_POINT('Ctrl Pts',(1.20577136594065,-15.5884572681209,1.8062444324207E-12));
#32618=CARTESIAN_POINT('Origin',(0.,0.,0.));
#32619=CARTESIAN_POINT('',(1.20577136594004,7.79422863405994,-13.5));
#32620=CARTESIAN_POINT('Ctrl Pts',(7.99123887912298E-16,11.6913429510899,
-6.75));
#32621=CARTESIAN_POINT('Ctrl Pts',(-1.88737914186277E-15,9.88268590217942,
-9.88268590218057));
#32622=CARTESIAN_POINT('Ctrl Pts',(1.20577136594065,7.79422863405889,-13.5000000000018));
#32623=CARTESIAN_POINT('Ctrl Pts',(1.20577136594065,7.79422863406204,-13.5));
#32624=CARTESIAN_POINT('Ctrl Pts',(-9.97494936421185E-17,3.61731409782101,
-13.5));
#32625=CARTESIAN_POINT('Ctrl Pts',(-2.13099703443277E-15,2.02444718271114E-14,
-13.5));
#32626=CARTESIAN_POINT('Origin',(0.,0.,0.));
#32627=CARTESIAN_POINT('',(1.20577136594005,-7.79422863405996,-13.5));
#32628=CARTESIAN_POINT('Ctrl Pts',(1.20577136594065,-7.79422863405891,-13.5000000000018));
#32629=CARTESIAN_POINT('Ctrl Pts',(6.79842967357653E-15,-9.88268590217943,
-9.88268590218058));
#32630=CARTESIAN_POINT('Ctrl Pts',(5.59386721538605E-15,-11.6913429510899,
-6.75000000000001));
#32631=CARTESIAN_POINT('Ctrl Pts',(-2.13099703443277E-15,2.02444718271114E-14,
-13.5));
#32632=CARTESIAN_POINT('Ctrl Pts',(-4.77395900588817E-15,-3.61731409782099,
-13.5));
#32633=CARTESIAN_POINT('Ctrl Pts',(1.20577136594065,-7.79422863406205,-13.5));
#32634=CARTESIAN_POINT('Origin',(10.,7.79422863405994,-13.5));
#32635=CARTESIAN_POINT('',(10.,-7.79422863405996,-13.5));
#32636=CARTESIAN_POINT('',(10.,7.79422863405994,-13.5));
#32637=CARTESIAN_POINT('Origin',(10.,-7.79422863405996,-13.5));
#32638=CARTESIAN_POINT('',(10.,-15.5884572681199,8.77615707241165E-17));
#32639=CARTESIAN_POINT('Origin',(10.,-15.5884572681199,8.77615707241165E-17));
#32640=CARTESIAN_POINT('',(10.,-7.79422863405994,13.5));
#32641=CARTESIAN_POINT('Origin',(10.,7.79422863405994,13.5));
#32642=CARTESIAN_POINT('',(10.,7.79422863405994,13.5));
#32643=CARTESIAN_POINT('Origin',(10.,15.5884572681199,0.));
#32644=CARTESIAN_POINT('',(10.,15.5884572681199,0.));
#32645=CARTESIAN_POINT('Origin',(10.,7.79422863405994,-13.5));
#32883=UNCERTAINTY_MEASURE_WITH_UNIT(LENGTH_MEASURE(0.01),#32904,
'DISTANCE_ACCURACY_VALUE',
'Maximum model space distance between geometric entities at asserted c
onnectivities');
#32886=UNCERTAINTY_MEASURE_WITH_UNIT(LENGTH_MEASURE(0.01),#32904,
'DISTANCE_ACCURACY_VALUE',
'Maximum model space distance between geometric entities at asserted c
onnectivities');
#32900=(
GEOMETRIC_REPRESENTATION_CONTEXT(3)
GLOBAL_UNCERTAINTY_ASSIGNED_CONTEXT((#32883))
GLOBAL_UNIT_ASSIGNED_CONTEXT((#32904,#32906,#32907))
REPRESENTATION_CONTEXT('','3D')
);
#32903=(
GEOMETRIC_REPRESENTATION_CONTEXT(3)
GLOBAL_UNCERTAINTY_ASSIGNED_CONTEXT((#32886))
GLOBAL_UNIT_ASSIGNED_CONTEXT((#32904,#32906,#32907))
REPRESENTATION_CONTEXT('','3D')
);
#32904=(
LENGTH_UNIT()
NAMED_UNIT(*)
SI_UNIT(.MILLI.,.METRE.)
);
#32906=(
NAMED_UNIT(*)
PLANE_ANGLE_UNIT()
SI_UNIT($,.RADIAN.)
);
#32907=(
NAMED_UNIT(*)
SI_UNIT($,.STERADIAN.)
SOLID_ANGLE_UNIT()
);
#32921=SHAPE_DEFINITION_REPRESENTATION(#32957,#33025);
#32957=PRODUCT_DEFINITION_SHAPE('',$,#33042);
#33025=SHAPE_REPRESENTATION('',(#17007),#32900);
#33028=PRODUCT_DEFINITION_CONTEXT('part definition',#33078,'design');
#33042=PRODUCT_DEFINITION(
'High Strength Hex Head Bolt DIN 6914 M16 x 60',
'High Strength Hex Head Bolt DIN 6914 M16 x 60',#33058,#33028);
#33058=PRODUCT_DEFINITION_FORMATION('',$,#33093);
#33078=APPLICATION_CONTEXT(
'Core Data for Automotive Mechanical Design Process');
#33079=PRODUCT_CONTEXT('part definition',#33078,'mechanical');
#33093=PRODUCT('High Strength Hex Head Bolt DIN 6914 M16 x 60',
'High Strength Hex Head Bolt DIN 6914 M16 x 60',$,(#33079));
#33099=PRESENTATION_STYLE_ASSIGNMENT((#33105));
#33105=SURFACE_STYLE_USAGE(.BOTH.,#33111);
#33111=SURFACE_SIDE_STYLE('',(#33117));
#33117=SURFACE_STYLE_FILL_AREA(#33123);
#33123=FILL_AREA_STYLE('Opaque(31,36,43)',(#33129));
#33129=FILL_AREA_STYLE_COLOUR('Opaque(31,36,43)',#33135);
#33135=COLOUR_RGB('Opaque(31,36,43)',0.12156862745098,0.141176470588235,
0.168627450980392);
ENDSEC;
END-ISO-10303-21;
